ISO-10303-21;
HEADER;
/* Generated by software containing ST-Developer
 * from STEP Tools, Inc. (www.steptools.com) 
 */

FILE_DESCRIPTION(
/* description */ ('Gravity roller conveyor section'),
/* implementation_level */ '2;1');

FILE_NAME(
/* name */ 'Cap Screw - M5x20.step',
/* time_stamp */ '2026-11-02T07:43:02-08:00',
/* author */ (''),
/* organization */ (''),
/* preprocessor_version */ 'ST-DEVELOPER v20.2',
/* originating_system */ 'Autodesk Translation Framework v15.17.0.0',
/* authorisation */ '');

FILE_SCHEMA (('AUTOMOTIVE_DESIGN { 1 0 10303 214 3 1 1 }'));
ENDSEC;

DATA;
#10=MECHANICAL_DESIGN_GEOMETRIC_PRESENTATION_REPRESENTATION('',(#534),#13821);
#410=CONICAL_SURFACE('',#8258,0.4,0.785398163397448);
#411=CONICAL_SURFACE('',#8262,0.41,0.785398163397448);
#412=CONICAL_SURFACE('',#8266,0.26,0.463647609000806);
#413=CONICAL_SURFACE('',#8270,0.225,0.785398163397448);
#426=ORIENTED_CLOSED_SHELL('',*,#7634,.F.);
#430=BREP_WITH_VOIDS('Body1',#7633,(#426));
#466=SHAPE_REPRESENTATION_RELATIONSHIP('SRR','None',#14003,#500);
#500=ADVANCED_BREP_SHAPE_REPRESENTATION('',(#430),#13790);
#534=STYLED_ITEM('',(#14193),#430);
#631=FACE_BOUND('',#1626,.T.);
#858=PLANE('',#8256);
#859=PLANE('',#8264);
#860=PLANE('',#8272);
#861=PLANE('',#8273);
#862=PLANE('',#8274);
#863=PLANE('',#8275);
#864=PLANE('',#8276);
#865=PLANE('',#8277);
#866=PLANE('',#8278);
#867=PLANE('',#8279);
#868=PLANE('',#8280);
#1180=FACE_OUTER_BOUND('',#1621,.T.);
#1181=FACE_OUTER_BOUND('',#1622,.T.);
#1182=FACE_OUTER_BOUND('',#1623,.T.);
#1183=FACE_OUTER_BOUND('',#1624,.T.);
#1184=FACE_OUTER_BOUND('',#1625,.T.);
#1185=FACE_OUTER_BOUND('',#1627,.T.);
#1186=FACE_OUTER_BOUND('',#1628,.T.);
#1187=FACE_OUTER_BOUND('',#1629,.T.);
#1188=FACE_OUTER_BOUND('',#1630,.T.);
#1189=FACE_OUTER_BOUND('',#1631,.T.);
#1190=FACE_OUTER_BOUND('',#1632,.T.);
#1191=FACE_OUTER_BOUND('',#1633,.T.);
#1192=FACE_OUTER_BOUND('',#1634,.T.);
#1193=FACE_OUTER_BOUND('',#1635,.T.);
#1194=FACE_OUTER_BOUND('',#1636,.T.);
#1195=FACE_OUTER_BOUND('',#1637,.T.);
#1196=FACE_OUTER_BOUND('',#1638,.T.);
#1621=EDGE_LOOP('',(#6166));
#1622=EDGE_LOOP('',(#6167,#6168,#6169,#6170));
#1623=EDGE_LOOP('',(#6171,#6172,#6173,#6174));
#1624=EDGE_LOOP('',(#6175,#6176,#6177,#6178));
#1625=EDGE_LOOP('',(#6179));
#1626=EDGE_LOOP('',(#6180));
#1627=EDGE_LOOP('',(#6181,#6182,#6183,#6184));
#1628=EDGE_LOOP('',(#6185,#6186,#6187,#6188));
#1629=EDGE_LOOP('',(#6189,#6190,#6191,#6192));
#1630=EDGE_LOOP('',(#6193));
#1631=EDGE_LOOP('',(#6194,#6195,#6196,#6197));
#1632=EDGE_LOOP('',(#6198,#6199,#6200,#6201));
#1633=EDGE_LOOP('',(#6202,#6203,#6204,#6205));
#1634=EDGE_LOOP('',(#6206,#6207,#6208,#6209));
#1635=EDGE_LOOP('',(#6210,#6211,#6212,#6213));
#1636=EDGE_LOOP('',(#6214,#6215,#6216,#6217));
#1637=EDGE_LOOP('',(#6218,#6219,#6220,#6221,#6222,#6223));
#1638=EDGE_LOOP('',(#6224,#6225,#6226,#6227,#6228,#6229));
#2383=LINE('',#12233,#3101);
#2384=LINE('',#12237,#3102);
#2385=LINE('',#12241,#3103);
#2386=LINE('',#12248,#3104);
#2387=LINE('',#12252,#3105);
#2388=LINE('',#12256,#3106);
#2389=LINE('',#12261,#3107);
#2390=LINE('',#12263,#3108);
#2391=LINE('',#12265,#3109);
#2392=LINE('',#12266,#3110);
#2393=LINE('',#12269,#3111);
#2394=LINE('',#12271,#3112);
#2395=LINE('',#12272,#3113);
#2396=LINE('',#12275,#3114);
#2397=LINE('',#12277,#3115);
#2398=LINE('',#12278,#3116);
#2399=LINE('',#12281,#3117);
#2400=LINE('',#12283,#3118);
#2401=LINE('',#12284,#3119);
#2402=LINE('',#12287,#3120);
#2403=LINE('',#12289,#3121);
#2404=LINE('',#12290,#3122);
#2405=LINE('',#12292,#3123);
#2406=LINE('',#12293,#3124);
#3101=VECTOR('',#9686,0.4);
#3102=VECTOR('',#9691,0.425);
#3103=VECTOR('',#9696,0.41);
#3104=VECTOR('',#9705,0.26);
#3105=VECTOR('',#9710,0.25);
#3106=VECTOR('',#9715,0.225);
#3107=VECTOR('',#9720,1.);
#3108=VECTOR('',#9721,1.);
#3109=VECTOR('',#9722,1.);
#3110=VECTOR('',#9723,1.);
#3111=VECTOR('',#9726,1.);
#3112=VECTOR('',#9727,1.);
#3113=VECTOR('',#9728,1.);
#3114=VECTOR('',#9731,1.);
#3115=VECTOR('',#9732,1.);
#3116=VECTOR('',#9733,1.);
#3117=VECTOR('',#9736,1.);
#3118=VECTOR('',#9737,1.);
#3119=VECTOR('',#9738,1.);
#3120=VECTOR('',#9741,1.);
#3121=VECTOR('',#9742,1.);
#3122=VECTOR('',#9743,1.);
#3123=VECTOR('',#9746,1.);
#3124=VECTOR('',#9747,1.);
#3401=CIRCLE('',#8257,0.375);
#3402=CIRCLE('',#8259,0.425);
#3403=CIRCLE('',#8261,0.425);
#3404=CIRCLE('',#8263,0.395);
#3405=CIRCLE('',#8265,0.27);
#3406=CIRCLE('',#8267,0.24505);
#3407=CIRCLE('',#8269,0.24505);
#3408=CIRCLE('',#8271,0.2);
#3911=VERTEX_POINT('',#12228);
#3912=VERTEX_POINT('',#12231);
#3913=VERTEX_POINT('',#12235);
#3914=VERTEX_POINT('',#12239);
#3915=VERTEX_POINT('',#12243);
#3916=VERTEX_POINT('',#12246);
#3917=VERTEX_POINT('',#12250);
#3918=VERTEX_POINT('',#12254);
#3919=VERTEX_POINT('',#12259);
#3920=VERTEX_POINT('',#12260);
#3921=VERTEX_POINT('',#12262);
#3922=VERTEX_POINT('',#12264);
#3923=VERTEX_POINT('',#12268);
#3924=VERTEX_POINT('',#12270);
#3925=VERTEX_POINT('',#12274);
#3926=VERTEX_POINT('',#12276);
#3927=VERTEX_POINT('',#12280);
#3928=VERTEX_POINT('',#12282);
#3929=VERTEX_POINT('',#12286);
#3930=VERTEX_POINT('',#12288);
#4720=EDGE_CURVE('',#3911,#3911,#3401,.T.);
#4721=EDGE_CURVE('',#3912,#3912,#3402,.T.);
#4722=EDGE_CURVE('',#3912,#3911,#2383,.T.);
#4723=EDGE_CURVE('',#3913,#3913,#3403,.T.);
#4724=EDGE_CURVE('',#3913,#3912,#2384,.T.);
#4725=EDGE_CURVE('',#3914,#3914,#3404,.T.);
#4726=EDGE_CURVE('',#3914,#3913,#2385,.T.);
#4727=EDGE_CURVE('',#3915,#3915,#3405,.T.);
#4728=EDGE_CURVE('',#3916,#3916,#3406,.F.);
#4729=EDGE_CURVE('',#3916,#3915,#2386,.T.);
#4730=EDGE_CURVE('',#3917,#3917,#3407,.F.);
#4731=EDGE_CURVE('',#3917,#3916,#2387,.T.);
#4732=EDGE_CURVE('',#3918,#3918,#3408,.T.);
#4733=EDGE_CURVE('',#3918,#3917,#2388,.T.);
#4734=EDGE_CURVE('',#3919,#3920,#2389,.T.);
#4735=EDGE_CURVE('',#3920,#3921,#2390,.T.);
#4736=EDGE_CURVE('',#3921,#3922,#2391,.T.);
#4737=EDGE_CURVE('',#3919,#3922,#2392,.T.);
#4738=EDGE_CURVE('',#3920,#3923,#2393,.T.);
#4739=EDGE_CURVE('',#3923,#3924,#2394,.T.);
#4740=EDGE_CURVE('',#3924,#3921,#2395,.T.);
#4741=EDGE_CURVE('',#3923,#3925,#2396,.T.);
#4742=EDGE_CURVE('',#3925,#3926,#2397,.T.);
#4743=EDGE_CURVE('',#3926,#3924,#2398,.T.);
#4744=EDGE_CURVE('',#3925,#3927,#2399,.T.);
#4745=EDGE_CURVE('',#3927,#3928,#2400,.T.);
#4746=EDGE_CURVE('',#3928,#3926,#2401,.T.);
#4747=EDGE_CURVE('',#3927,#3929,#2402,.T.);
#4748=EDGE_CURVE('',#3929,#3930,#2403,.T.);
#4749=EDGE_CURVE('',#3930,#3928,#2404,.T.);
#4750=EDGE_CURVE('',#3929,#3919,#2405,.T.);
#4751=EDGE_CURVE('',#3922,#3930,#2406,.T.);
#6166=ORIENTED_EDGE('',*,*,#4720,.F.);
#6167=ORIENTED_EDGE('',*,*,#4721,.F.);
#6168=ORIENTED_EDGE('',*,*,#4722,.T.);
#6169=ORIENTED_EDGE('',*,*,#4720,.T.);
#6170=ORIENTED_EDGE('',*,*,#4722,.F.);
#6171=ORIENTED_EDGE('',*,*,#4723,.F.);
#6172=ORIENTED_EDGE('',*,*,#4724,.T.);
#6173=ORIENTED_EDGE('',*,*,#4721,.T.);
#6174=ORIENTED_EDGE('',*,*,#4724,.F.);
#6175=ORIENTED_EDGE('',*,*,#4725,.F.);
#6176=ORIENTED_EDGE('',*,*,#4726,.T.);
#6177=ORIENTED_EDGE('',*,*,#4723,.T.);
#6178=ORIENTED_EDGE('',*,*,#4726,.F.);
#6179=ORIENTED_EDGE('',*,*,#4725,.T.);
#6180=ORIENTED_EDGE('',*,*,#4727,.F.);
#6181=ORIENTED_EDGE('',*,*,#4728,.F.);
#6182=ORIENTED_EDGE('',*,*,#4729,.T.);
#6183=ORIENTED_EDGE('',*,*,#4727,.T.);
#6184=ORIENTED_EDGE('',*,*,#4729,.F.);
#6185=ORIENTED_EDGE('',*,*,#4730,.F.);
#6186=ORIENTED_EDGE('',*,*,#4731,.T.);
#6187=ORIENTED_EDGE('',*,*,#4728,.T.);
#6188=ORIENTED_EDGE('',*,*,#4731,.F.);
#6189=ORIENTED_EDGE('',*,*,#4732,.F.);
#6190=ORIENTED_EDGE('',*,*,#4733,.T.);
#6191=ORIENTED_EDGE('',*,*,#4730,.T.);
#6192=ORIENTED_EDGE('',*,*,#4733,.F.);
#6193=ORIENTED_EDGE('',*,*,#4732,.T.);
#6194=ORIENTED_EDGE('',*,*,#4734,.T.);
#6195=ORIENTED_EDGE('',*,*,#4735,.T.);
#6196=ORIENTED_EDGE('',*,*,#4736,.T.);
#6197=ORIENTED_EDGE('',*,*,#4737,.F.);
#6198=ORIENTED_EDGE('',*,*,#4738,.T.);
#6199=ORIENTED_EDGE('',*,*,#4739,.T.);
#6200=ORIENTED_EDGE('',*,*,#4740,.T.);
#6201=ORIENTED_EDGE('',*,*,#4735,.F.);
#6202=ORIENTED_EDGE('',*,*,#4741,.T.);
#6203=ORIENTED_EDGE('',*,*,#4742,.T.);
#6204=ORIENTED_EDGE('',*,*,#4743,.T.);
#6205=ORIENTED_EDGE('',*,*,#4739,.F.);
#6206=ORIENTED_EDGE('',*,*,#4744,.T.);
#6207=ORIENTED_EDGE('',*,*,#4745,.T.);
#6208=ORIENTED_EDGE('',*,*,#4746,.T.);
#6209=ORIENTED_EDGE('',*,*,#4742,.F.);
#6210=ORIENTED_EDGE('',*,*,#4747,.T.);
#6211=ORIENTED_EDGE('',*,*,#4748,.T.);
#6212=ORIENTED_EDGE('',*,*,#4749,.T.);
#6213=ORIENTED_EDGE('',*,*,#4745,.F.);
#6214=ORIENTED_EDGE('',*,*,#4750,.T.);
#6215=ORIENTED_EDGE('',*,*,#4737,.T.);
#6216=ORIENTED_EDGE('',*,*,#4751,.T.);
#6217=ORIENTED_EDGE('',*,*,#4748,.F.);
#6218=ORIENTED_EDGE('',*,*,#4750,.F.);
#6219=ORIENTED_EDGE('',*,*,#4747,.F.);
#6220=ORIENTED_EDGE('',*,*,#4744,.F.);
#6221=ORIENTED_EDGE('',*,*,#4741,.F.);
#6222=ORIENTED_EDGE('',*,*,#4738,.F.);
#6223=ORIENTED_EDGE('',*,*,#4734,.F.);
#6224=ORIENTED_EDGE('',*,*,#4751,.F.);
#6225=ORIENTED_EDGE('',*,*,#4736,.F.);
#6226=ORIENTED_EDGE('',*,*,#4740,.F.);
#6227=ORIENTED_EDGE('',*,*,#4743,.F.);
#6228=ORIENTED_EDGE('',*,*,#4746,.F.);
#6229=ORIENTED_EDGE('',*,*,#4749,.F.);
#7144=CYLINDRICAL_SURFACE('',#8260,0.425);
#7145=CYLINDRICAL_SURFACE('',#8268,0.24505);
#7381=ADVANCED_FACE('',(#1180),#858,.T.);
#7382=ADVANCED_FACE('',(#1181),#410,.T.);
#7383=ADVANCED_FACE('',(#1182),#7144,.T.);
#7384=ADVANCED_FACE('',(#1183),#411,.T.);
#7385=ADVANCED_FACE('',(#1184,#631),#859,.T.);
#7386=ADVANCED_FACE('',(#1185),#412,.T.);
#7387=ADVANCED_FACE('',(#1186),#7145,.T.);
#7388=ADVANCED_FACE('',(#1187),#413,.T.);
#7389=ADVANCED_FACE('',(#1188),#860,.T.);
#7390=ADVANCED_FACE('',(#1189),#861,.F.);
#7391=ADVANCED_FACE('',(#1190),#862,.F.);
#7392=ADVANCED_FACE('',(#1191),#863,.F.);
#7393=ADVANCED_FACE('',(#1192),#864,.F.);
#7394=ADVANCED_FACE('',(#1193),#865,.F.);
#7395=ADVANCED_FACE('',(#1194),#866,.F.);
#7396=ADVANCED_FACE('',(#1195),#867,.F.);
#7397=ADVANCED_FACE('',(#1196),#868,.F.);
#7633=CLOSED_SHELL('',(#7381,#7382,#7383,#7384,#7385,#7386,#7387,#7388,
#7389));
#7634=CLOSED_SHELL('',(#7390,#7391,#7392,#7393,#7394,#7395,#7396,#7397));
#8255=AXIS2_PLACEMENT_3D('',#12226,#9676,#9677);
#8256=AXIS2_PLACEMENT_3D('',#12227,#9678,#9679);
#8257=AXIS2_PLACEMENT_3D('',#12229,#9680,#9681);
#8258=AXIS2_PLACEMENT_3D('',#12230,#9682,#9683);
#8259=AXIS2_PLACEMENT_3D('',#12232,#9684,#9685);
#8260=AXIS2_PLACEMENT_3D('',#12234,#9687,#9688);
#8261=AXIS2_PLACEMENT_3D('',#12236,#9689,#9690);
#8262=AXIS2_PLACEMENT_3D('',#12238,#9692,#9693);
#8263=AXIS2_PLACEMENT_3D('',#12240,#9694,#9695);
#8264=AXIS2_PLACEMENT_3D('',#12242,#9697,#9698);
#8265=AXIS2_PLACEMENT_3D('',#12244,#9699,#9700);
#8266=AXIS2_PLACEMENT_3D('',#12245,#9701,#9702);
#8267=AXIS2_PLACEMENT_3D('',#12247,#9703,#9704);
#8268=AXIS2_PLACEMENT_3D('',#12249,#9706,#9707);
#8269=AXIS2_PLACEMENT_3D('',#12251,#9708,#9709);
#8270=AXIS2_PLACEMENT_3D('',#12253,#9711,#9712);
#8271=AXIS2_PLACEMENT_3D('',#12255,#9713,#9714);
#8272=AXIS2_PLACEMENT_3D('',#12257,#9716,#9717);
#8273=AXIS2_PLACEMENT_3D('',#12258,#9718,#9719);
#8274=AXIS2_PLACEMENT_3D('',#12267,#9724,#9725);
#8275=AXIS2_PLACEMENT_3D('',#12273,#9729,#9730);
#8276=AXIS2_PLACEMENT_3D('',#12279,#9734,#9735);
#8277=AXIS2_PLACEMENT_3D('',#12285,#9739,#9740);
#8278=AXIS2_PLACEMENT_3D('',#12291,#9744,#9745);
#8279=AXIS2_PLACEMENT_3D('',#12294,#9748,#9749);
#8280=AXIS2_PLACEMENT_3D('',#12295,#9750,#9751);
#9676=DIRECTION('axis',(0.,0.,1.));
#9677=DIRECTION('refdir',(1.,0.,0.));
#9678=DIRECTION('center_axis',(0.,1.,0.));
#9679=DIRECTION('ref_axis',(0.,0.,1.));
#9680=DIRECTION('center_axis',(0.,-1.,0.));
#9681=DIRECTION('ref_axis',(1.,0.,0.));
#9682=DIRECTION('center_axis',(0.,-1.,0.));
#9683=DIRECTION('ref_axis',(1.,0.,0.));
#9684=DIRECTION('center_axis',(0.,-1.,0.));
#9685=DIRECTION('ref_axis',(1.,0.,0.));
#9686=DIRECTION('',(0.707106781186548,0.707106781186547,8.65956056235493E-17));
#9687=DIRECTION('center_axis',(0.,-1.,0.));
#9688=DIRECTION('ref_axis',(1.,0.,0.));
#9689=DIRECTION('center_axis',(0.,-1.,0.));
#9690=DIRECTION('ref_axis',(1.,0.,0.));
#9691=DIRECTION('',(0.,1.,0.));
#9692=DIRECTION('center_axis',(0.,1.,0.));
#9693=DIRECTION('ref_axis',(1.,0.,0.));
#9694=DIRECTION('center_axis',(0.,-1.,0.));
#9695=DIRECTION('ref_axis',(1.,0.,0.));
#9696=DIRECTION('',(-0.707106781186547,0.707106781186548,-8.65956056235493E-17));
#9697=DIRECTION('center_axis',(0.,-1.,0.));
#9698=DIRECTION('ref_axis',(0.,0.,-1.));
#9699=DIRECTION('center_axis',(0.,-1.,0.));
#9700=DIRECTION('ref_axis',(1.,0.,0.));
#9701=DIRECTION('center_axis',(0.,1.,0.));
#9702=DIRECTION('ref_axis',(1.,0.,0.));
#9703=DIRECTION('center_axis',(0.,1.,0.));
#9704=DIRECTION('ref_axis',(1.,0.,0.));
#9705=DIRECTION('',(-0.447213595499958,0.894427190999916,-5.47678698264203E-17));
#9706=DIRECTION('center_axis',(0.,-1.,0.));
#9707=DIRECTION('ref_axis',(1.,0.,0.));
#9708=DIRECTION('center_axis',(0.,1.,0.));
#9709=DIRECTION('ref_axis',(1.,0.,0.));
#9710=DIRECTION('',(0.,1.,0.));
#9711=DIRECTION('center_axis',(0.,1.,0.));
#9712=DIRECTION('ref_axis',(1.,0.,0.));
#9713=DIRECTION('center_axis',(0.,-1.,0.));
#9714=DIRECTION('ref_axis',(1.,0.,0.));
#9715=DIRECTION('',(-0.707106781186547,0.707106781186548,-8.65956056235493E-17));
#9716=DIRECTION('center_axis',(0.,-1.,0.));
#9717=DIRECTION('ref_axis',(0.,0.,-1.));
#9718=DIRECTION('center_axis',(0.866025403784439,0.,-0.5));
#9719=DIRECTION('ref_axis',(0.5,0.,0.866025403784439));
#9720=DIRECTION('',(-0.5,0.,-0.866025403784439));
#9721=DIRECTION('',(0.,-1.,0.));
#9722=DIRECTION('',(0.5,0.,0.866025403784439));
#9723=DIRECTION('',(0.,-1.,0.));
#9724=DIRECTION('center_axis',(1.20185167898973E-16,0.,-1.));
#9725=DIRECTION('ref_axis',(1.,0.,1.20185167898973E-16));
#9726=DIRECTION('',(-1.,0.,-1.20185167898973E-16));
#9727=DIRECTION('',(0.,-1.,0.));
#9728=DIRECTION('',(1.,0.,1.20185167898973E-16));
#9729=DIRECTION('center_axis',(-0.866025403784439,0.,-0.5));
#9730=DIRECTION('ref_axis',(0.5,0.,-0.866025403784439));
#9731=DIRECTION('',(-0.5,0.,0.866025403784439));
#9732=DIRECTION('',(0.,-1.,0.));
#9733=DIRECTION('',(0.5,0.,-0.866025403784439));
#9734=DIRECTION('center_axis',(-0.866025403784439,0.,0.5));
#9735=DIRECTION('ref_axis',(-0.5,0.,-0.866025403784439));
#9736=DIRECTION('',(0.5,0.,0.866025403784439));
#9737=DIRECTION('',(0.,-1.,0.));
#9738=DIRECTION('',(-0.5,0.,-0.866025403784439));
#9739=DIRECTION('center_axis',(-2.40370335797945E-16,0.,1.));
#9740=DIRECTION('ref_axis',(-1.,0.,-2.40370335797945E-16));
#9741=DIRECTION('',(1.,0.,2.40370335797945E-16));
#9742=DIRECTION('',(0.,-1.,0.));
#9743=DIRECTION('',(-1.,0.,-2.40370335797945E-16));
#9744=DIRECTION('center_axis',(0.866025403784439,0.,0.5));
#9745=DIRECTION('ref_axis',(-0.5,0.,0.866025403784439));
#9746=DIRECTION('',(0.5,0.,-0.866025403784439));
#9747=DIRECTION('',(-0.5,0.,0.866025403784439));
#9748=DIRECTION('center_axis',(0.,1.,0.));
#9749=DIRECTION('ref_axis',(1.,0.,0.));
#9750=DIRECTION('center_axis',(0.,-1.,0.));
#9751=DIRECTION('ref_axis',(0.,0.,-1.));
#12226=CARTESIAN_POINT('',(0.,0.,0.));
#12227=CARTESIAN_POINT('Origin',(0.375,0.5,0.));
#12228=CARTESIAN_POINT('',(-0.375,0.5,-4.59242549680257E-17));
#12229=CARTESIAN_POINT('Origin',(0.,0.5,0.));
#12230=CARTESIAN_POINT('Origin',(0.,0.475,0.));
#12231=CARTESIAN_POINT('',(-0.425,0.45,-5.20474889637625E-17));
#12232=CARTESIAN_POINT('Origin',(0.,0.45,0.));
#12233=CARTESIAN_POINT('',(-0.4,0.475,-4.89858719658941E-17));
#12234=CARTESIAN_POINT('Origin',(0.,0.24,0.));
#12235=CARTESIAN_POINT('',(-0.425,0.0299999999999998,-5.20474889637625E-17));
#12236=CARTESIAN_POINT('Origin',(0.,0.0299999999999998,0.));
#12237=CARTESIAN_POINT('',(-0.425,0.24,-5.20474889637625E-17));
#12238=CARTESIAN_POINT('Origin',(0.,0.0150000000000001,0.));
#12239=CARTESIAN_POINT('',(-0.395,4.85722573273506E-17,-4.83735485663204E-17));
#12240=CARTESIAN_POINT('Origin',(0.,0.,0.));
#12241=CARTESIAN_POINT('',(-0.41,0.0150000000000001,-5.02105187650415E-17));
#12242=CARTESIAN_POINT('Origin',(0.27,0.,0.));
#12243=CARTESIAN_POINT('',(-0.27,0.,-3.30654635769785E-17));
#12244=CARTESIAN_POINT('Origin',(0.,0.,0.));
#12245=CARTESIAN_POINT('Origin',(0.,-0.02,0.));
#12246=CARTESIAN_POINT('',(-0.24505,-0.0498999999999999,3.00099698131059E-17));
#12247=CARTESIAN_POINT('Origin',(0.,-0.0498999999999999,0.));
#12248=CARTESIAN_POINT('',(-0.26,-0.02,-3.18408167778312E-17));
#12249=CARTESIAN_POINT('Origin',(0.,-0.995,0.));
#12250=CARTESIAN_POINT('',(-0.24505,-1.95495,3.00099698131059E-17));
#12251=CARTESIAN_POINT('Origin',(0.,-1.95495,0.));
#12252=CARTESIAN_POINT('',(-0.24505,-0.995,-3.00099698131059E-17));
#12253=CARTESIAN_POINT('Origin',(0.,-1.975,0.));
#12254=CARTESIAN_POINT('',(-0.2,-2.,-2.44929359829471E-17));
#12255=CARTESIAN_POINT('Origin',(0.,-2.,0.));
#12256=CARTESIAN_POINT('',(-0.225,-1.975,-2.75545529808154E-17));
#12257=CARTESIAN_POINT('Origin',(0.,-2.,0.));
#12258=CARTESIAN_POINT('Origin',(0.115470053837925,-0.5,-0.2));
#12259=CARTESIAN_POINT('',(0.23094010767585,-0.5,0.));
#12260=CARTESIAN_POINT('',(0.115470053837925,-0.5,-0.2));
#12261=CARTESIAN_POINT('',(0.23094010767585,-0.5,0.));
#12262=CARTESIAN_POINT('',(0.115470053837925,-0.8,-0.2));
#12263=CARTESIAN_POINT('',(0.115470053837925,-0.5,-0.2));
#12264=CARTESIAN_POINT('',(0.23094010767585,-0.8,0.));
#12265=CARTESIAN_POINT('',(0.23094010767585,-0.8,0.));
#12266=CARTESIAN_POINT('',(0.23094010767585,-0.5,0.));
#12267=CARTESIAN_POINT('Origin',(-0.115470053837925,-0.5,-0.2));
#12268=CARTESIAN_POINT('',(-0.115470053837925,-0.5,-0.2));
#12269=CARTESIAN_POINT('',(0.115470053837925,-0.5,-0.2));
#12270=CARTESIAN_POINT('',(-0.115470053837925,-0.8,-0.2));
#12271=CARTESIAN_POINT('',(-0.115470053837925,-0.5,-0.2));
#12272=CARTESIAN_POINT('',(0.115470053837925,-0.8,-0.2));
#12273=CARTESIAN_POINT('Origin',(-0.23094010767585,-0.5,-2.77555756156289E-17));
#12274=CARTESIAN_POINT('',(-0.23094010767585,-0.5,-2.82820063659975E-17));
#12275=CARTESIAN_POINT('',(-0.115470053837925,-0.5,-0.2));
#12276=CARTESIAN_POINT('',(-0.23094010767585,-0.8,-2.77555756156289E-17));
#12277=CARTESIAN_POINT('',(-0.23094010767585,-0.5,-2.82820063659975E-17));
#12278=CARTESIAN_POINT('',(-0.115470053837925,-0.8,-0.2));
#12279=CARTESIAN_POINT('Origin',(-0.115470053837925,-0.5,0.2));
#12280=CARTESIAN_POINT('',(-0.115470053837925,-0.5,0.2));
#12281=CARTESIAN_POINT('',(-0.23094010767585,-0.5,-2.82820063659975E-17));
#12282=CARTESIAN_POINT('',(-0.115470053837925,-0.8,0.2));
#12283=CARTESIAN_POINT('',(-0.115470053837925,-0.5,0.2));
#12284=CARTESIAN_POINT('',(-0.23094010767585,-0.8,-2.82820063659975E-17));
#12285=CARTESIAN_POINT('Origin',(0.115470053837925,-0.5,0.2));
#12286=CARTESIAN_POINT('',(0.115470053837925,-0.5,0.2));
#12287=CARTESIAN_POINT('',(-0.115470053837925,-0.5,0.2));
#12288=CARTESIAN_POINT('',(0.115470053837925,-0.8,0.2));
#12289=CARTESIAN_POINT('',(0.115470053837925,-0.5,0.2));
#12290=CARTESIAN_POINT('',(-0.115470053837925,-0.8,0.2));
#12291=CARTESIAN_POINT('Origin',(0.23094010767585,-0.5,0.));
#12292=CARTESIAN_POINT('',(0.115470053837925,-0.5,0.2));
#12293=CARTESIAN_POINT('',(0.115470053837925,-0.8,0.2));
#12294=CARTESIAN_POINT('Origin',(0.,-0.5,0.));
#12295=CARTESIAN_POINT('Origin',(0.,-0.8,0.));
#13751=UNCERTAINTY_MEASURE_WITH_UNIT(LENGTH_MEASURE(0.001),#13822,
'DISTANCE_ACCURACY_VALUE',
'Maximum model space distance between geometric entities at asserted c
onnectivities');
#13782=UNCERTAINTY_MEASURE_WITH_UNIT(LENGTH_MEASURE(0.001),#13822,
'DISTANCE_ACCURACY_VALUE',
'Maximum model space distance between geometric entities at asserted c
onnectivities');
#13790=(
GEOMETRIC_REPRESENTATION_CONTEXT(3)
GLOBAL_UNCERTAINTY_ASSIGNED_CONTEXT((#13751))
GLOBAL_UNIT_ASSIGNED_CONTEXT((#13822,#13824,#13825))
REPRESENTATION_CONTEXT('','3D')
);
#13821=(
GEOMETRIC_REPRESENTATION_CONTEXT(3)
GLOBAL_UNCERTAINTY_ASSIGNED_CONTEXT((#13782))
GLOBAL_UNIT_ASSIGNED_CONTEXT((#13822,#13824,#13825))
REPRESENTATION_CONTEXT('','3D')
);
#13822=(
LENGTH_UNIT()
NAMED_UNIT(*)
SI_UNIT(.CENTI.,.METRE.)
);
#13824=(
NAMED_UNIT(*)
PLANE_ANGLE_UNIT()
SI_UNIT($,.RADIAN.)
);
#13825=(
NAMED_UNIT(*)
SI_UNIT($,.STERADIAN.)
SOLID_ANGLE_UNIT()
);
#13833=SHAPE_DEFINITION_REPRESENTATION(#13871,#14003);
#13871=PRODUCT_DEFINITION_SHAPE('',$,#14042);
#14003=SHAPE_REPRESENTATION('',(#8255),#13790);
#14034=PRODUCT_DEFINITION_CONTEXT('part definition',#14150,'design');
#14042=PRODUCT_DEFINITION('Cap Screw - M5x20','Cap Screw - M5x20',#14080,
#14034);
#14080=PRODUCT_DEFINITION_FORMATION('',$,#14159);
#14150=APPLICATION_CONTEXT(
'Core Data for Automotive Mechanical Design Process');
#14151=PRODUCT_CONTEXT('part definition',#14150,'mechanical');
#14159=PRODUCT('Cap Screw - M5x20','Cap Screw - M5x20',
'Cap Screw - M5x20',(#14151));
#14193=PRESENTATION_STYLE_ASSIGNMENT((#14198));
#14198=SURFACE_STYLE_USAGE(.BOTH.,#14203);
#14203=SURFACE_SIDE_STYLE('',(#14208));
#14208=SURFACE_STYLE_FILL_AREA(#14213);
#14213=FILL_AREA_STYLE('CAD Library Painted - Graphite',(#14218));
#14218=FILL_AREA_STYLE_COLOUR('CAD Library Painted - Graphite',#14223);
#14223=COLOUR_RGB('CAD Library Painted - Graphite',0.168627450980392,0.192156862745098,
0.231372549019608);
ENDSEC;
END-ISO-10303-21;
